ISO-10303-21;
HEADER;
/* Generated by software containing ST-Developer
 * from STEP Tools, Inc. (www.steptools.com) 
 */

FILE_DESCRIPTION(
/* description */ ('Worm-less right-angle friction wheel drive'),
/* implementation_level */ '2;1');

FILE_NAME(
/* name */ 'Front spring seat (1).step',
/* time_stamp */ '2026-10-28T03:22:36-07:00',
/* author */ (''),
/* organization */ (''),
/* preprocessor_version */ 'ST-DEVELOPER v20.2',
/* originating_system */ 'Autodesk Translation Framework v15.17.0.0',
/* authorisation */ '');

FILE_SCHEMA (('AUTOMOTIVE_DESIGN { 1 0 10303 214 3 1 1 }'));
ENDSEC;

DATA;
#10=MECHANICAL_DESIGN_GEOMETRIC_PRESENTATION_REPRESENTATION('',(#631),#17046);
#537=SHAPE_REPRESENTATION_RELATIONSHIP('SRR','None',#17280,#584);
#584=ADVANCED_BREP_SHAPE_REPRESENTATION('',(#685),#17016);
#631=STYLED_ITEM('',(#17591),#685);
#685=MANIFOLD_SOLID_BREP('Body1',#8186);
#1062=PLANE('',#9222);
#1063=PLANE('',#9223);
#1433=FACE_OUTER_BOUND('',#2089,.T.);
#1434=FACE_OUTER_BOUND('',#2090,.T.);
#1435=FACE_OUTER_BOUND('',#2091,.T.);
#2089=EDGE_LOOP('',(#6584,#6585,#6586,#6587));
#2090=EDGE_LOOP('',(#6588));
#2091=EDGE_LOOP('',(#6589));
#2671=LINE('',#14413,#3211);
#3211=VECTOR('',#11025,0.7);
#3687=CIRCLE('',#9220,0.7);
#3688=CIRCLE('',#9221,0.7);
#4219=VERTEX_POINT('',#14410);
#4220=VERTEX_POINT('',#14412);
#5061=EDGE_CURVE('',#4219,#4219,#3687,.T.);
#5062=EDGE_CURVE('',#4219,#4220,#2671,.T.);
#5063=EDGE_CURVE('',#4220,#4220,#3688,.T.);
#6584=ORIENTED_EDGE('',*,*,#5061,.F.);
#6585=ORIENTED_EDGE('',*,*,#5062,.T.);
#6586=ORIENTED_EDGE('',*,*,#5063,.T.);
#6587=ORIENTED_EDGE('',*,*,#5062,.F.);
#6588=ORIENTED_EDGE('',*,*,#5061,.T.);
#6589=ORIENTED_EDGE('',*,*,#5063,.F.);
#7644=CYLINDRICAL_SURFACE('',#9219,0.7);
#7925=ADVANCED_FACE('',(#1433),#7644,.T.);
#7926=ADVANCED_FACE('',(#1434),#1062,.T.);
#7927=ADVANCED_FACE('',(#1435),#1063,.F.);
#8186=CLOSED_SHELL('',(#7925,#7926,#7927));
#9218=AXIS2_PLACEMENT_3D('',#14408,#11019,#11020);
#9219=AXIS2_PLACEMENT_3D('',#14409,#11021,#11022);
#9220=AXIS2_PLACEMENT_3D('',#14411,#11023,#11024);
#9221=AXIS2_PLACEMENT_3D('',#14414,#11026,#11027);
#9222=AXIS2_PLACEMENT_3D('',#14415,#11028,#11029);
#9223=AXIS2_PLACEMENT_3D('',#14416,#11030,#11031);
#11019=DIRECTION('axis',(0.,0.,1.));
#11020=DIRECTION('refdir',(1.,0.,0.));
#11021=DIRECTION('center_axis',(0.,1.,0.));
#11022=DIRECTION('ref_axis',(1.,0.,0.));
#11023=DIRECTION('center_axis',(0.,1.,0.));
#11024=DIRECTION('ref_axis',(1.,0.,0.));
#11025=DIRECTION('',(0.,-1.,0.));
#11026=DIRECTION('center_axis',(0.,1.,0.));
#11027=DIRECTION('ref_axis',(1.,0.,0.));
#11028=DIRECTION('center_axis',(0.,1.,0.));
#11029=DIRECTION('ref_axis',(1.,0.,0.));
#11030=DIRECTION('center_axis',(0.,1.,0.));
#11031=DIRECTION('ref_axis',(1.,0.,0.));
#14408=CARTESIAN_POINT('',(0.,0.,0.));
#14409=CARTESIAN_POINT('Origin',(5.5,5.4,4.));
#14410=CARTESIAN_POINT('',(4.8,5.7,4.));
#14411=CARTESIAN_POINT('Origin',(5.5,5.7,4.));
#14412=CARTESIAN_POINT('',(4.8,5.4,4.));
#14413=CARTESIAN_POINT('',(4.8,5.4,4.));
#14414=CARTESIAN_POINT('Origin',(5.5,5.4,4.));
#14415=CARTESIAN_POINT('Origin',(5.5,5.7,4.));
#14416=CARTESIAN_POINT('Origin',(5.5,5.4,4.));
#16963=UNCERTAINTY_MEASURE_WITH_UNIT(LENGTH_MEASURE(0.001),#17047,
'DISTANCE_ACCURACY_VALUE',
'Maximum model space distance between geometric entities at asserted c
onnectivities');
#16993=UNCERTAINTY_MEASURE_WITH_UNIT(LENGTH_MEASURE(0.001),#17047,
'DISTANCE_ACCURACY_VALUE',
'Maximum model space distance between geometric entities at asserted c
onnectivities');
#17016=(
GEOMETRIC_REPRESENTATION_CONTEXT(3)
GLOBAL_UNCERTAINTY_ASSIGNED_CONTEXT((#16963))
GLOBAL_UNIT_ASSIGNED_CONTEXT((#17047,#17049,#17050))
REPRESENTATION_CONTEXT('','3D')
);
#17046=(
GEOMETRIC_REPRESENTATION_CONTEXT(3)
GLOBAL_UNCERTAINTY_ASSIGNED_CONTEXT((#16993))
GLOBAL_UNIT_ASSIGNED_CONTEXT((#17047,#17049,#17050))
REPRESENTATION_CONTEXT('','3D')
);
#17047=(
LENGTH_UNIT()
NAMED_UNIT(*)
SI_UNIT(.CENTI.,.METRE.)
);
#17049=(
NAMED_UNIT(*)
PLANE_ANGLE_UNIT()
SI_UNIT($,.RADIAN.)
);
#17050=(
NAMED_UNIT(*)
SI_UNIT($,.STERADIAN.)
SOLID_ANGLE_UNIT()
);
#17073=SHAPE_DEFINITION_REPRESENTATION(#17125,#17280);
#17125=PRODUCT_DEFINITION_SHAPE('',$,#17333);
#17280=SHAPE_REPRESENTATION('',(#9218),#17016);
#17310=PRODUCT_DEFINITION_CONTEXT('part definition',#17468,'design');
#17333=PRODUCT_DEFINITION('Front spring seat (1)','Front spring seat (1)',
#17385,#17310);
#17385=PRODUCT_DEFINITION_FORMATION('',$,#17492);
#17468=APPLICATION_CONTEXT(
'Core Data for Automotive Mechanical Design Process');
#17469=PRODUCT_CONTEXT('part definition',#17468,'mechanical');
#17492=PRODUCT('Front spring seat (1)','Front spring seat (1)',
'Front spring seat (1)',(#17469));
#17585=COLOUR_RGB('Grey',0.48,0.52,0.57);
#17586=FILL_AREA_STYLE_COLOUR('',#17585);
#17587=FILL_AREA_STYLE('',(#17586));
#17588=SURFACE_STYLE_FILL_AREA(#17587);
#17589=SURFACE_SIDE_STYLE('',(#17588));
#17590=SURFACE_STYLE_USAGE(.BOTH.,#17589);
#17591=PRESENTATION_STYLE_ASSIGNMENT((#17590));
ENDSEC;
END-ISO-10303-21;
